ISO-10303-21;
HEADER;
/* Generated by software containing ST-Developer
 * from STEP Tools, Inc. (www.steptools.com) 
 */

FILE_DESCRIPTION(
/* description */ ('Single-Axis Profile-Rail Linear Slide'),
/* implementation_level */ '2;1');

FILE_NAME(
/* name */ 'Flat Washer - M6.step',
/* time_stamp */ '2026-10-27T10:47:43-07:00',
/* author */ (''),
/* organization */ (''),
/* preprocessor_version */ 'ST-DEVELOPER v20.2',
/* originating_system */ 'Autodesk Translation Framework v15.17.0.0',
/* authorisation */ '');

FILE_SCHEMA (('AUTOMOTIVE_DESIGN { 1 0 10303 214 3 1 1 }'));
ENDSEC;

DATA;
#10=MECHANICAL_DESIGN_GEOMETRIC_PRESENTATION_REPRESENTATION('',(#354),#14478);
#300=SHAPE_REPRESENTATION_RELATIONSHIP('SRR','None',#14632,#327);
#327=ADVANCED_BREP_SHAPE_REPRESENTATION('',(#377),#14476);
#354=STYLED_ITEM('',(#14838),#377);
#377=MANIFOLD_SOLID_BREP('Body1',#8618);
#465=FACE_BOUND('',#1819,.T.);
#466=FACE_BOUND('',#1821,.T.);
#827=PLANE('',#9575);
#828=PLANE('',#9576);
#1274=FACE_OUTER_BOUND('',#1816,.T.);
#1275=FACE_OUTER_BOUND('',#1817,.T.);
#1276=FACE_OUTER_BOUND('',#1818,.T.);
#1277=FACE_OUTER_BOUND('',#1820,.T.);
#1816=EDGE_LOOP('',(#7995,#7996,#7997,#7998));
#1817=EDGE_LOOP('',(#7999,#8000,#8001,#8002));
#1818=EDGE_LOOP('',(#8003));
#1819=EDGE_LOOP('',(#8004));
#1820=EDGE_LOOP('',(#8005));
#1821=EDGE_LOOP('',(#8006));
#2785=LINE('',#14317,#3756);
#2786=LINE('',#14323,#3757);
#3756=VECTOR('',#11870,0.32);
#3757=VECTOR('',#11877,0.6);
#3926=CIRCLE('',#9570,0.32);
#3927=CIRCLE('',#9571,0.32);
#3928=CIRCLE('',#9573,0.6);
#3929=CIRCLE('',#9574,0.6);
#4660=VERTEX_POINT('',#14314);
#4661=VERTEX_POINT('',#14316);
#4662=VERTEX_POINT('',#14320);
#4663=VERTEX_POINT('',#14322);
#5775=EDGE_CURVE('',#4660,#4660,#3926,.T.);
#5776=EDGE_CURVE('',#4660,#4661,#2785,.T.);
#5777=EDGE_CURVE('',#4661,#4661,#3927,.T.);
#5778=EDGE_CURVE('',#4662,#4662,#3928,.T.);
#5779=EDGE_CURVE('',#4662,#4663,#2786,.T.);
#5780=EDGE_CURVE('',#4663,#4663,#3929,.T.);
#7995=ORIENTED_EDGE('',*,*,#5775,.F.);
#7996=ORIENTED_EDGE('',*,*,#5776,.T.);
#7997=ORIENTED_EDGE('',*,*,#5777,.T.);
#7998=ORIENTED_EDGE('',*,*,#5776,.F.);
#7999=ORIENTED_EDGE('',*,*,#5778,.F.);
#8000=ORIENTED_EDGE('',*,*,#5779,.T.);
#8001=ORIENTED_EDGE('',*,*,#5780,.T.);
#8002=ORIENTED_EDGE('',*,*,#5779,.F.);
#8003=ORIENTED_EDGE('',*,*,#5778,.T.);
#8004=ORIENTED_EDGE('',*,*,#5775,.T.);
#8005=ORIENTED_EDGE('',*,*,#5780,.F.);
#8006=ORIENTED_EDGE('',*,*,#5777,.F.);
#8130=CYLINDRICAL_SURFACE('',#9569,0.32);
#8131=CYLINDRICAL_SURFACE('',#9572,0.6);
#8568=ADVANCED_FACE('',(#1274),#8130,.F.);
#8569=ADVANCED_FACE('',(#1275),#8131,.T.);
#8570=ADVANCED_FACE('',(#1276,#465),#827,.T.);
#8571=ADVANCED_FACE('',(#1277,#466),#828,.F.);
#8618=CLOSED_SHELL('',(#8568,#8569,#8570,#8571));
#9568=AXIS2_PLACEMENT_3D('',#14312,#11864,#11865);
#9569=AXIS2_PLACEMENT_3D('',#14313,#11866,#11867);
#9570=AXIS2_PLACEMENT_3D('',#14315,#11868,#11869);
#9571=AXIS2_PLACEMENT_3D('',#14318,#11871,#11872);
#9572=AXIS2_PLACEMENT_3D('',#14319,#11873,#11874);
#9573=AXIS2_PLACEMENT_3D('',#14321,#11875,#11876);
#9574=AXIS2_PLACEMENT_3D('',#14324,#11878,#11879);
#9575=AXIS2_PLACEMENT_3D('',#14325,#11880,#11881);
#9576=AXIS2_PLACEMENT_3D('',#14326,#11882,#11883);
#11864=DIRECTION('axis',(0.,0.,1.));
#11865=DIRECTION('refdir',(1.,0.,0.));
#11866=DIRECTION('center_axis',(0.,1.,0.));
#11867=DIRECTION('ref_axis',(1.,0.,0.));
#11868=DIRECTION('center_axis',(0.,-1.,0.));
#11869=DIRECTION('ref_axis',(1.,0.,0.));
#11870=DIRECTION('',(0.,-1.,0.));
#11871=DIRECTION('center_axis',(0.,-1.,0.));
#11872=DIRECTION('ref_axis',(1.,0.,0.));
#11873=DIRECTION('center_axis',(0.,1.,0.));
#11874=DIRECTION('ref_axis',(1.,0.,0.));
#11875=DIRECTION('center_axis',(0.,1.,0.));
#11876=DIRECTION('ref_axis',(1.,0.,0.));
#11877=DIRECTION('',(0.,-1.,0.));
#11878=DIRECTION('center_axis',(0.,1.,0.));
#11879=DIRECTION('ref_axis',(1.,0.,0.));
#11880=DIRECTION('center_axis',(0.,1.,0.));
#11881=DIRECTION('ref_axis',(1.,0.,0.));
#11882=DIRECTION('center_axis',(0.,1.,0.));
#11883=DIRECTION('ref_axis',(1.,0.,0.));
#14312=CARTESIAN_POINT('',(0.,0.,0.));
#14313=CARTESIAN_POINT('Origin',(0.,0.,0.));
#14314=CARTESIAN_POINT('',(-0.32,0.16,3.91886975727153E-17));
#14315=CARTESIAN_POINT('Origin',(0.,0.16,0.));
#14316=CARTESIAN_POINT('',(-0.32,0.,3.91886975727153E-17));
#14317=CARTESIAN_POINT('',(-0.32,0.,3.91886975727153E-17));
#14318=CARTESIAN_POINT('Origin',(0.,0.,0.));
#14319=CARTESIAN_POINT('Origin',(0.,0.,0.));
#14320=CARTESIAN_POINT('',(-0.6,0.16,7.34788079488412E-17));
#14321=CARTESIAN_POINT('Origin',(0.,0.16,0.));
#14322=CARTESIAN_POINT('',(-0.6,0.,7.34788079488412E-17));
#14323=CARTESIAN_POINT('',(-0.6,0.,7.34788079488412E-17));
#14324=CARTESIAN_POINT('Origin',(0.,0.,0.));
#14325=CARTESIAN_POINT('Origin',(0.,0.16,0.));
#14326=CARTESIAN_POINT('Origin',(0.,0.,0.));
#14444=UNCERTAINTY_MEASURE_WITH_UNIT(LENGTH_MEASURE(0.001),#14479,
'DISTANCE_ACCURACY_VALUE',
'Maximum model space distance between geometric entities at asserted c
onnectivities');
#14446=UNCERTAINTY_MEASURE_WITH_UNIT(LENGTH_MEASURE(0.001),#14479,
'DISTANCE_ACCURACY_VALUE',
'Maximum model space distance between geometric entities at asserted c
onnectivities');
#14476=(
GEOMETRIC_REPRESENTATION_CONTEXT(3)
GLOBAL_UNCERTAINTY_ASSIGNED_CONTEXT((#14444))
GLOBAL_UNIT_ASSIGNED_CONTEXT((#14479,#14481,#14482))
REPRESENTATION_CONTEXT('','3D')
);
#14478=(
GEOMETRIC_REPRESENTATION_CONTEXT(3)
GLOBAL_UNCERTAINTY_ASSIGNED_CONTEXT((#14446))
GLOBAL_UNIT_ASSIGNED_CONTEXT((#14479,#14481,#14482))
REPRESENTATION_CONTEXT('','3D')
);
#14479=(
LENGTH_UNIT()
NAMED_UNIT(*)
SI_UNIT(.CENTI.,.METRE.)
);
#14481=(
NAMED_UNIT(*)
PLANE_ANGLE_UNIT()
SI_UNIT($,.RADIAN.)
);
#14482=(
NAMED_UNIT(*)
SI_UNIT($,.STERADIAN.)
SOLID_ANGLE_UNIT()
);
#14512=SHAPE_DEFINITION_REPRESENTATION(#14583,#14632);
#14583=PRODUCT_DEFINITION_SHAPE('',$,#14664);
#14632=SHAPE_REPRESENTATION('',(#9568),#14476);
#14634=PRODUCT_DEFINITION_CONTEXT('part definition',#14729,'design');
#14664=PRODUCT_DEFINITION('Flat Washer - M6','Flat Washer - M6',#14695,
#14634);
#14695=PRODUCT_DEFINITION_FORMATION('',$,#14760);
#14729=APPLICATION_CONTEXT(
'Core Data for Automotive Mechanical Design Process');
#14730=PRODUCT_CONTEXT('part definition',#14729,'mechanical');
#14760=PRODUCT('Flat Washer - M6','Flat Washer - M6','Flat Washer - M6',
(#14730));
#14832=COLOUR_RGB('Black',0.12,0.14,0.17);
#14833=FILL_AREA_STYLE_COLOUR('',#14832);
#14834=FILL_AREA_STYLE('',(#14833));
#14835=SURFACE_STYLE_FILL_AREA(#14834);
#14836=SURFACE_SIDE_STYLE('',(#14835));
#14837=SURFACE_STYLE_USAGE(.BOTH.,#14836);
#14838=PRESENTATION_STYLE_ASSIGNMENT((#14837));
ENDSEC;
END-ISO-10303-21;
